ISO-10303-21;
HEADER;
FILE_DESCRIPTION (('STEP AP214'),
    '1' );
FILE_NAME ('socket button head screw_iso_ISO 7380 - M3 x 6 - 6N.step',
    '2026-10-26T05:17:54',
    ( '' ),
    ( '' ),
    'SwSTEP 2.0',
    'SolidWorks 2026',
    '' );
FILE_SCHEMA (( 'AUTOMOTIVE_DESIGN' ));
ENDSEC;

DATA;
#12=ADVANCED_FACE ( 'NONE', ( #2550 ), #5478, .T. ) ;
#30=VECTOR ( 'NONE', #11564, 1000.000000000000114 ) ;
#34=EDGE_CURVE ( 'NONE', #7938, #5032, #4885, .T. ) ;
#81=EDGE_CURVE ( 'NONE', #9930, #10652, #10526, .T. ) ;
#87=PLANE ( 'NONE',  #9136 ) ;
#105=AXIS2_PLACEMENT_3D ( 'NONE', #1700, #5689, #8636 ) ;
#109=EDGE_CURVE ( 'NONE', #7067, #112, #11947, .T. ) ;
#112=VERTEX_POINT ( 'NONE', #12017 ) ;
#118=EDGE_LOOP ( 'NONE', ( #5135, #6023 ) ) ;
#119=DIRECTION ( 'NONE',  ( 0.000000000000000000, 0.5000000000000000000, -0.8660254037844385966 ) ) ;
#130=ORIENTED_EDGE ( 'NONE', *, *, #2719, .F. ) ;
#131=CARTESIAN_POINT ( 'NONE',  ( 1.040000000000000036, 0.5773502691896263972, -1.000000000000000000 ) ) ;
#149=EDGE_CURVE ( 'NONE', #10256, #6226, #4830, .T. ) ;
#150=FACE_OUTER_BOUND ( 'NONE', #10972, .T. ) ;
#156=VECTOR ( 'NONE', #8810, 1000.000000000000000 ) ;
#163=( LENGTH_UNIT ( ) NAMED_UNIT ( * ) SI_UNIT ( .MILLI., .METRE. ) );
#172=AXIS2_PLACEMENT_3D ( 'NONE', #7936, #11922, #10932 ) ;
#224=ORIENTED_EDGE ( 'NONE', *, *, #6026, .F. ) ;
#225=DIRECTION ( 'NONE',  ( -0.000000000000000000, 0.000000000000000000, -1.000000000000000000 ) ) ;
#236=ORIENTED_EDGE ( 'NONE', *, *, #952, .F. ) ;
#242=VERTEX_POINT ( 'NONE', #9265 ) ;
#243=CARTESIAN_POINT ( 'NONE',  ( 4.336808689942017736E-16, 0.000000000000000000, 0.000000000000000000 ) ) ;
#247=DIRECTION ( 'NONE',  ( 0.000000000000000000, 0.000000000000000000, 1.000000000000000000 ) ) ;
#261=VERTEX_POINT ( 'NONE', #1283 ) ;
#262=FACE_OUTER_BOUND ( 'NONE', #6852, .T. ) ;
#270=AXIS2_PLACEMENT_3D ( 'NONE', #2486, #11695, #10523 ) ;
#278=ORIENTED_EDGE ( 'NONE', *, *, #5223, .F. ) ;
#343=LINE ( 'NONE', #3380, #2212 ) ;
#365=LINE ( 'NONE', #2416, #4028 ) ;
#380=DIRECTION ( 'NONE',  ( -1.000000000000000000, -0.000000000000000000, -0.000000000000000000 ) ) ;
#402=CARTESIAN_POINT ( 'NONE',  ( 1.750000000000000000, 0.000000000000000000, 0.000000000000000000 ) ) ;
#410=AXIS2_PLACEMENT_3D ( 'NONE', #10816, #609, #2848 ) ;
#421=CARTESIAN_POINT ( 'NONE',  ( 0.000000000000000000, 0.5773502691896263972, -1.000000000000000000 ) ) ;
#423=EDGE_LOOP ( 'NONE', ( #4044, #8845, #2488, #12293, #6036, #11034 ) ) ;
#424=SHAPE_REPRESENTATION_RELATIONSHIP ( 'NONE' , 'NONE' ,  #9523, #10270 ) ;
#441=EDGE_LOOP ( 'NONE', ( #236, #7328, #3929 ) ) ;
#475=ORIENTED_EDGE ( 'NONE', *, *, #517, .T. ) ;
#496=LINE ( 'NONE', #7448, #8208 ) ;
#517=EDGE_CURVE ( 'NONE', #7067, #10542, #2603, .T. ) ;
#520=ORIENTED_EDGE ( 'NONE', *, *, #6993, .F. ) ;
#529=CARTESIAN_POINT ( 'NONE',  ( 1.040000000000000036, 0.000000000000000000, 0.000000000000000000 ) ) ;
#538=CARTESIAN_POINT ( 'NONE',  ( 3.033375984251970081, -8.673617379884035472E-16, 0.000000000000000000 ) ) ;
#609=DIRECTION ( 'NONE',  ( -1.000000000000000000, -0.000000000000000000, -0.000000000000000000 ) ) ;
#689=ORIENTED_EDGE ( 'NONE', *, *, #1063, .F. ) ;
#702=CARTESIAN_POINT ( 'NONE',  ( 0.000000000000000000, 0.000000000000000000, 1.499999999999999556 ) ) ;
#708=PRODUCT_DEFINITION_FORMATION_WITH_SPECIFIED_SOURCE ( 'ANY', '', #2726, .NOT_KNOWN. ) ;
#740=CARTESIAN_POINT ( 'NONE',  ( 1.617350269189632428, 0.000000000000000000, 0.000000000000000000 ) ) ;
#746=ORIENTED_EDGE ( 'NONE', *, *, #952, .T. ) ;
#755=EDGE_LOOP ( 'NONE', ( #10469, #5474, #7145, #11199 ) ) ;
#766=PLANE ( 'NONE',  #12339 ) ;
#775=ORIENTED_EDGE ( 'NONE', *, *, #2311, .F. ) ;
#797=DIRECTION ( 'NONE',  ( 0.000000000000000000, 0.000000000000000000, 1.000000000000000000 ) ) ;
#799=DIRECTION ( 'NONE',  ( 0.000000000000000000, 0.000000000000000000, 1.000000000000000000 ) ) ;
#800=FACE_OUTER_BOUND ( 'NONE', #9608, .T. ) ;
#833=DIRECTION ( 'NONE',  ( -1.000000000000000000, -0.000000000000000000, -0.000000000000000000 ) ) ;
#850=CARTESIAN_POINT ( 'NONE',  ( 1.750000000000000000, 0.000000000000000000, 1.499999999999999556 ) ) ;
#874=DIRECTION ( 'NONE',  ( -1.000000000000000000, -0.000000000000000000, -0.000000000000000000 ) ) ;
#887=DIRECTION ( 'NONE',  ( -0.000000000000000000, 0.000000000000000000, 1.000000000000000000 ) ) ;
#909=ORIENTED_EDGE ( 'NONE', *, *, #6026, .T. ) ;
#910=FACE_OUTER_BOUND ( 'NONE', #4176, .T. ) ;
#937=DIRECTION ( 'NONE',  ( 0.000000000000000000, 0.000000000000000000, 1.000000000000000000 ) ) ;
#952=EDGE_CURVE ( 'NONE', #10652, #7727, #7415, .T. ) ;
#962=ORIENTED_EDGE ( 'NONE', *, *, #8949, .F. ) ;
#977=VERTEX_POINT ( 'NONE', #2845 ) ;
#987=EDGE_CURVE ( 'NONE', #10383, #11518, #2907, .T. ) ;
#1016=EDGE_CURVE ( 'NONE', #11762, #12580, #2408, .T. ) ;
#1017=CARTESIAN_POINT ( 'NONE',  ( 1.040000000000000036, 0.000000000000000000, 0.000000000000000000 ) ) ;
#1034=VECTOR ( 'NONE', #3985, 1000.000000000000000 ) ;
#1040=DIRECTION ( 'NONE',  ( -1.000000000000000000, -0.000000000000000000, -0.000000000000000000 ) ) ;
#1056=PLANE ( 'NONE',  #12390 ) ;
#1063=EDGE_CURVE ( 'NONE', #11446, #10328, #11590, .T. ) ;
#1105=DIRECTION ( 'NONE',  ( 0.000000000000000000, 0.000000000000000000, 1.000000000000000000 ) ) ;
#1122=ORIENTED_EDGE ( 'NONE', *, *, #81, .F. ) ;
#1173=ORIENTED_EDGE ( 'NONE', *, *, #6921, .F. ) ;
#1192=CARTESIAN_POINT ( 'NONE',  ( 1.617350269189632428, 0.000000000000000000, 0.000000000000000000 ) ) ;
#1214=DIRECTION ( 'NONE',  ( -1.000000000000000000, -0.000000000000000000, -0.000000000000000000 ) ) ;
#1239=AXIS2_PLACEMENT_3D ( 'NONE', #7208, #5306, #5243 ) ;
#1259=ORIENTED_EDGE ( 'NONE', *, *, #11539, .T. ) ;
#1263=CARTESIAN_POINT ( 'NONE',  ( 3.033375984251970081, -8.673617379884035472E-16, 0.000000000000000000 ) ) ;
#1283=CARTESIAN_POINT ( 'NONE',  ( 1.040000000000000036, 0.8660254037844390407, 0.5000000000000002220 ) ) ;
#1288=SURFACE_STYLE_FILL_AREA ( #1483 ) ;
#1306=FACE_OUTER_BOUND ( 'NONE', #7469, .T. ) ;
#1347=AXIS2_PLACEMENT_3D ( 'NONE', #6885, #3700, #797 ) ;
#1384=ORIENTED_EDGE ( 'NONE', *, *, #3350, .F. ) ;
#1396=DIRECTION ( 'NONE',  ( 0.000000000000000000, -0.5000000000000003331, 0.8660254037844383745 ) ) ;
#1398=DIRECTION ( 'NONE',  ( 1.000000000000000000, 0.000000000000000000, 0.000000000000000000 ) ) ;
#1416=AXIS2_PLACEMENT_3D ( 'NONE', #12045, #10076, #4203 ) ;
#1433=ORIENTED_EDGE ( 'NONE', *, *, #9842, .F. ) ;
#1483=FILL_AREA_STYLE ('',( #6388 ) ) ;
#1553=ORIENTED_EDGE ( 'NONE', *, *, #8758, .T. ) ;
#1589=DIRECTION ( 'NONE',  ( -1.000000000000000000, -0.000000000000000000, -0.000000000000000000 ) ) ;
#1599=CARTESIAN_POINT ( 'NONE',  ( 1.040000000000000036, -0.5773502691896253980, -1.000000000000000000 ) ) ;
#1604=ADVANCED_FACE ( 'NONE', ( #11357 ), #3197, .F. ) ;
#1682=LINE ( 'NONE', #2863, #2317 ) ;
#1700=CARTESIAN_POINT ( 'NONE',  ( 1.040000000000000036, -1.154700538379251684, -1.199226976249124676E-17 ) ) ;
#1752=CARTESIAN_POINT ( 'NONE',  ( 1.269999999999999796, 0.000000000000000000, 0.000000000000000000 ) ) ;
#1753=CARTESIAN_POINT ( 'NONE',  ( 1.269999999999999796, 0.000000000000000000, 0.000000000000000000 ) ) ;
#1763=CARTESIAN_POINT ( 'NONE',  ( 1.649999999999999911, 0.000000000000000000, 2.849999999999999645 ) ) ;
#1831=EDGE_CURVE ( 'NONE', #6585, #11492, #9090, .T. ) ;
#1856=DIRECTION ( 'NONE',  ( 0.000000000000000000, 0.000000000000000000, 1.000000000000000000 ) ) ;
#1878=FACE_OUTER_BOUND ( 'NONE', #11584, .T. ) ;
#1884=DIRECTION ( 'NONE',  ( -1.000000000000000000, -0.000000000000000000, -0.000000000000000000 ) ) ;
#1890=LINE ( 'NONE', #9865, #5546 ) ;
#1900=ORIENTED_EDGE ( 'NONE', *, *, #7233, .F. ) ;
#1907=DIRECTION ( 'NONE',  ( -1.000000000000000000, -0.000000000000000000, -0.000000000000000000 ) ) ;
#1933=DIRECTION ( 'NONE',  ( 0.000000000000000000, -1.000000000000000000, 0.000000000000000000 ) ) ;
#1944=CARTESIAN_POINT ( 'NONE',  ( 1.040000000000000036, 1.154700538379252350, -1.084202172485497162E-16 ) ) ;
#1953=AXIS2_PLACEMENT_3D ( 'NONE', #2238, #4065, #6012 ) ;
#1973=DIRECTION ( 'NONE',  ( -0.000000000000000000, 0.5000000000000003331, -0.8660254037844383745 ) ) ;
#1985=DIRECTION ( 'NONE',  ( -1.000000000000000000, -0.000000000000000000, -0.000000000000000000 ) ) ;
#2001=DIRECTION ( 'NONE',  ( 0.000000000000000000, 0.000000000000000000, -1.000000000000000000 ) ) ;
#2045=DIRECTION ( 'NONE',  ( 0.000000000000000000, 0.000000000000000000, 1.000000000000000000 ) ) ;
#2053=ORIENTED_EDGE ( 'NONE', *, *, #11546, .T. ) ;
#2060=VECTOR ( 'NONE', #11693, 1000.000000000000000 ) ;
#2061=CARTESIAN_POINT ( 'NONE',  ( 0.000000000000000000, 1.154700538379252350, -1.084202172485497162E-16 ) ) ;
#2063=LINE ( 'NONE', #6770, #3657 ) ;
#2086=EDGE_CURVE ( 'NONE', #977, #10652, #343, .T. ) ;
#2097=DIRECTION ( 'NONE',  ( 0.000000000000000000, 0.000000000000000000, 1.000000000000000000 ) ) ;
#2098=ORIENTED_EDGE ( 'NONE', *, *, #7758, .F. ) ;
#2105=CARTESIAN_POINT ( 'NONE',  ( 1.040000000000000036, -0.5773502691896253980, -1.000000000000000000 ) ) ;
#2121=UNCERTAINTY_MEASURE_WITH_UNIT (LENGTH_MEASURE( 1.000000000000000082E-05 ), #3271, 'distance_accuracy_value', 'NONE');
#2155=CARTESIAN_POINT ( 'NONE',  ( 1.040000000000000036, -1.154700538379251684, 0.000000000000000000 ) ) ;
#2160=CIRCLE ( 'NONE', #6333, 1.425000000000000044 ) ;
#2175=AXIS2_PLACEMENT_3D ( 'NONE', #1017, #5014, #6849 ) ;
#2193=ADVANCED_FACE ( 'NONE', ( #12593 ), #3441, .T. ) ;
#2196=TOROIDAL_SURFACE ( 'NONE', #9294, 1.599999999999999645, 0.1000000000000000056 ) ;
#2198=DIRECTION ( 'NONE',  ( 0.000000000000000000, 0.000000000000000000, 1.000000000000000000 ) ) ;
#2212=VECTOR ( 'NONE', #11144, 1000.000000000000114 ) ;
#2238=CARTESIAN_POINT ( 'NONE',  ( 0.000000000000000000, 0.000000000000000000, 0.000000000000000000 ) ) ;
#2248=EDGE_CURVE ( 'NONE', #7938, #6066, #5129, .T. ) ;
#2263=CIRCLE ( 'NONE', #8318, 3.351416843938785028 ) ;
#2264=CARTESIAN_POINT ( 'NONE',  ( 1.649999999999999911, 1.959434878635764737E-16, -1.599999999999999645 ) ) ;
#2295=ORIENTED_EDGE ( 'NONE', *, *, #987, .F. ) ;
#2303=EDGE_LOOP ( 'NONE', ( #10656, #8806, #2505, #6000, #130 ) ) ;
#2311=EDGE_CURVE ( 'NONE', #9930, #5561, #6433, .T. ) ;
#2317=VECTOR ( 'NONE', #10830, 999.9999999999998863 ) ;
#2351=DIRECTION ( 'NONE',  ( -1.000000000000000000, 0.000000000000000000, -0.000000000000000000 ) ) ;
#2359=SHAPE_DEFINITION_REPRESENTATION ( #10327, #9523 ) ;
#2363=ORIENTED_EDGE ( 'NONE', *, *, #11691, .T. ) ;
#2367=DIRECTION ( 'NONE',  ( 0.000000000000000000, 0.000000000000000000, 1.000000000000000000 ) ) ;
#2375=DIRECTION ( 'NONE',  ( -1.000000000000000000, 0.000000000000000000, -0.000000000000000000 ) ) ;
#2398=VERTEX_POINT ( 'NONE', #12911 ) ;
#2400=EDGE_CURVE ( 'NONE', #12580, #11762, #8278, .T. ) ;
#2408=CIRCLE ( 'NONE', #1347, 2.849999999999999645 ) ;
#2416=CARTESIAN_POINT ( 'NONE',  ( 1.040000000000000036, 1.154700538379252350, -1.084202172485497162E-16 ) ) ;
#2417=DIRECTION ( 'NONE',  ( -0.000000000000000000, -0.5000000000000000000, 0.8660254037844385966 ) ) ;
#2420=PRODUCT_DEFINITION_CONTEXT ( 'detailed design', #7683, 'design' ) ;
#2461=DIRECTION ( 'NONE',  ( 0.000000000000000000, 0.000000000000000000, 1.000000000000000000 ) ) ;
#2466=CONICAL_SURFACE ( 'NONE', #12491, 1.219500000000000028, 0.7853981633974487231 ) ;
#2476=SURFACE_STYLE_USAGE ( .BOTH. , #3333 ) ;
#2483=CARTESIAN_POINT ( 'NONE',  ( 4.336808689942017736E-16, -1.425000000000000044, -2.617682533177466553E-16 ) ) ;
#2484=VERTEX_POINT ( 'NONE', #131 ) ;
#2486=CARTESIAN_POINT ( 'NONE',  ( 1.040000000000000036, -0.5773502691896253980, 1.000000000000000000 ) ) ;
#2488=ORIENTED_EDGE ( 'NONE', *, *, #12869, .T. ) ;
#2494=FACE_OUTER_BOUND ( 'NONE', #11714, .T. ) ;
#2505=ORIENTED_EDGE ( 'NONE', *, *, #3170, .T. ) ;
#2547=CARTESIAN_POINT ( 'NONE',  ( 1.040000000000000036, 0.5773502691896263972, 1.000000000000000000 ) ) ;
#2549=DIRECTION ( 'NONE',  ( -1.000000000000000000, -0.000000000000000000, -0.000000000000000000 ) ) ;
#2550=FACE_OUTER_BOUND ( 'NONE', #5796, .T. ) ;
#2584=DIRECTION ( 'NONE',  ( 0.000000000000000000, 1.224646799147353207E-16, -1.000000000000000000 ) ) ;
#2587=EDGE_CURVE ( 'NONE', #2398, #3791, #6541, .T. ) ;
#2588=ORIENTED_EDGE ( 'NONE', *, *, #11621, .F. ) ;
#2603=CIRCLE ( 'NONE', #9700, 1.000000000000000000 ) ;
#2611=DIRECTION ( 'NONE',  ( -1.000000000000000000, -0.000000000000000000, -0.000000000000000000 ) ) ;
#2621=ADVANCED_FACE ( 'NONE', ( #8331 ), #1056, .F. ) ;
#2646=AXIS2_PLACEMENT_3D ( 'NONE', #7873, #6756, #799 ) ;
#2677=CARTESIAN_POINT ( 'NONE',  ( 1.040000000000000036, -1.154700538379251684, -1.199226976249124676E-17 ) ) ;
#2678=ADVANCED_FACE ( 'NONE', ( #3218 ), #12170, .T. ) ;
#2696=UNCERTAINTY_MEASURE_WITH_UNIT (LENGTH_MEASURE( 1.000000000000000082E-05 ), #163, 'distance_accuracy_value', 'NONE');
#2703=ORIENTED_EDGE ( 'NONE', *, *, #5308, .F. ) ;
#2719=EDGE_CURVE ( 'NONE', #6066, #4728, #2160, .T. ) ;
#2726=PRODUCT ( 'socket button head screw_iso_ISO 7380 - M3 x 6 - 6N', 'socket button head screw_iso_ISO 7380 - M3 x 6 - 6N', '', ( #8245 ) ) ;
#2736=CIRCLE ( 'NONE', #172, 1.499999999999999778 ) ;
#2778=DIRECTION ( 'NONE',  ( -1.000000000000000000, -0.000000000000000000, -0.000000000000000000 ) ) ;
#2786=CARTESIAN_POINT ( 'NONE',  ( 1.269999999999999796, 0.000000000000000000, 2.849999999999999645 ) ) ;
#2813=CIRCLE ( 'NONE', #8451, 1.425000000000000044 ) ;
#2840=DIRECTION ( 'NONE',  ( -1.000000000000000000, -0.000000000000000000, -0.000000000000000000 ) ) ;
#2845=CARTESIAN_POINT ( 'NONE',  ( 1.040000000000000036, -0.5773502691896253980, 1.000000000000000000 ) ) ;
#2848=DIRECTION ( 'NONE',  ( 0.000000000000000000, 0.000000000000000000, 1.000000000000000000 ) ) ;
#2857=DIRECTION ( 'NONE',  ( -0.000000000000000000, -0.5000000000000003331, -0.8660254037844383745 ) ) ;
#2863=CARTESIAN_POINT ( 'NONE',  ( 7.650000000000000355, 1.493456771560197319E-16, -1.219500000000000028 ) ) ;
#2907=LINE ( 'NONE', #3954, #7624 ) ;
#2929=ORIENTED_EDGE ( 'NONE', *, *, #11621, .T. ) ;
#2934=DIRECTION ( 'NONE',  ( -0.000000000000000000, 0.5000000000000000000, 0.8660254037844385966 ) ) ;
#2962=AXIS2_PLACEMENT_3D ( 'NONE', #4327, #6341, #119 ) ;
#2991=FACE_OUTER_BOUND ( 'NONE', #8772, .T. ) ;
#3009=VECTOR ( 'NONE', #4890, 1000.000000000000227 ) ;
#3081=AXIS2_PLACEMENT_3D ( 'NONE', #11941, #5917, #3912 ) ;
#3125=AXIS2_PLACEMENT_3D ( 'NONE', #8782, #9827, #11661 ) ;
#3170=EDGE_CURVE ( 'NONE', #5032, #242, #7642, .T. ) ;
#3176=AXIS2_PLACEMENT_3D ( 'NONE', #8251, #8122, #12173 ) ;
#3197=PLANE ( 'NONE',  #4913 ) ;
#3198=LINE ( 'NONE', #6981, #1034 ) ;
#3206=EDGE_CURVE ( 'NONE', #112, #6226, #11352, .T. ) ;
#3208=CARTESIAN_POINT ( 'NONE',  ( 1.040000000000000036, -1.154700538379251684, -1.199226976249124676E-17 ) ) ;
#3218=FACE_OUTER_BOUND ( 'NONE', #10325, .T. ) ;
#3233=ORIENTED_EDGE ( 'NONE', *, *, #12643, .F. ) ;
#3246=ADVANCED_FACE ( 'NONE', ( #2494 ), #12566, .T. ) ;
#3255=AXIS2_PLACEMENT_3D ( 'NONE', #1753, #1884, #3920 ) ;
#3271=( LENGTH_UNIT ( ) NAMED_UNIT ( * ) SI_UNIT ( .MILLI., .METRE. ) );
#3333=SURFACE_SIDE_STYLE ('',( #1288 ) ) ;
#3340=PLANE ( 'NONE',  #4245 ) ;
#3350=EDGE_CURVE ( 'NONE', #5561, #8524, #1890, .T. ) ;
#3370=CARTESIAN_POINT ( 'NONE',  ( 0.000000000000000000, -1.154700538379251684, -1.199226976249124676E-17 ) ) ;
#3380=CARTESIAN_POINT ( 'NONE',  ( 1.040000000000000036, -1.154700538379251684, -1.199226976249124676E-17 ) ) ;
#3404=ORIENTED_EDGE ( 'NONE', *, *, #11539, .F. ) ;
#3434=COLOUR_RGB ( '',1.000000000000000000, 0.9490196078431372140, 0.9098039215686274384 ) ;
#3437=CLOSED_SHELL ( 'NONE', ( #11559, #4000, #4960, #11672, #2678, #4536, #8783, #4670, #6197, #9442, #2193, #11247, #12663, #8303, #3246, #7961, #7011, #7239, #11712, #12, #10976, #1604, #9427, #5787, #2621, #4785, #10788 ) ) ;
#3441=CYLINDRICAL_SURFACE ( 'NONE', #9516, 1.499999999999999556 ) ;
#3446=ORIENTED_EDGE ( 'NONE', *, *, #7865, .T. ) ;
#3491=ORIENTED_EDGE ( 'NONE', *, *, #7233, .T. ) ;
#3553=ORIENTED_EDGE ( 'NONE', *, *, #12602, .T. ) ;
#3558=ORIENTED_EDGE ( 'NONE', *, *, #3170, .F. ) ;
#3594=LINE ( 'NONE', #7576, #30 ) ;
#3636=DIRECTION ( 'NONE',  ( 0.000000000000000000, 1.000000000000000000, 1.224646799147353207E-16 ) ) ;
#3645=AXIS2_PLACEMENT_3D ( 'NONE', #1752, #8628, #12622 ) ;
#3652=DIRECTION ( 'NONE',  ( -0.000000000000000000, 1.000000000000000000, -0.000000000000000000 ) ) ;
#3657=VECTOR ( 'NONE', #2857, 1000.000000000000114 ) ;
#3700=DIRECTION ( 'NONE',  ( -1.000000000000000000, -0.000000000000000000, -0.000000000000000000 ) ) ;
#3722=CARTESIAN_POINT ( 'NONE',  ( 1.040000000000000036, 0.000000000000000000, 0.000000000000000000 ) ) ;
#3737=AXIS2_PLACEMENT_3D ( 'NONE', #3722, #2549, #12559 ) ;
#3772=VECTOR ( 'NONE', #833, 1000.000000000000000 ) ;
#3783=ORIENTED_EDGE ( 'NONE', *, *, #5308, .T. ) ;
#3791=VERTEX_POINT ( 'NONE', #12140 ) ;
#3850=PLANE ( 'NONE',  #10621 ) ;
#3863=EDGE_LOOP ( 'NONE', ( #10855, #7117 ) ) ;
#3870=ORIENTED_EDGE ( 'NONE', *, *, #2400, .T. ) ;
#3872=PRODUCT_DEFINITION ( 'UNKNOWN', '', #708, #2420 ) ;
#3881=LINE ( 'NONE', #5040, #10887 ) ;
#3912=DIRECTION ( 'NONE',  ( 0.000000000000000000, 1.000000000000000000, 0.000000000000000000 ) ) ;
#3920=DIRECTION ( 'NONE',  ( 0.000000000000000000, 0.000000000000000000, 1.000000000000000000 ) ) ;
#3929=ORIENTED_EDGE ( 'NONE', *, *, #6752, .F. ) ;
#3932=CARTESIAN_POINT ( 'NONE',  ( 1.649999999999999911, 3.490243377569956061E-16, -2.849999999999999645 ) ) ;
#3954=CARTESIAN_POINT ( 'NONE',  ( 0.000000000000000000, -0.5773502691896253980, 1.000000000000000000 ) ) ;
#3955=EDGE_LOOP ( 'NONE', ( #6679, #6593 ) ) ;
#3985=DIRECTION ( 'NONE',  ( -1.000000000000000000, 0.000000000000000000, 0.000000000000000000 ) ) ;
#3995=DIRECTION ( 'NONE',  ( 1.000000000000000000, 0.000000000000000000, -0.000000000000000000 ) ) ;
#4000=ADVANCED_FACE ( 'NONE', ( #8544 ), #5150, .F. ) ;
#4017=DIRECTION ( 'NONE',  ( -0.5000000000000042188, 0.000000000000000000, 0.8660254037844361541 ) ) ;
#4027=DIRECTION ( 'NONE',  ( -1.000000000000000000, -0.000000000000000000, -0.000000000000000000 ) ) ;
#4028=VECTOR ( 'NONE', #5349, 1000.000000000000227 ) ;
#4044=ORIENTED_EDGE ( 'NONE', *, *, #987, .T. ) ;
#4063=( GEOMETRIC_REPRESENTATION_CONTEXT ( 3 ) GLOBAL_UNCERTAINTY_ASSIGNED_CONTEXT ( ( #11132 ) ) GLOBAL_UNIT_ASSIGNED_CONTEXT ( ( #10316, #8424, #9400 ) ) REPRESENTATION_CONTEXT ( 'NONE', 'WORKASPACE' ) );
#4065=DIRECTION ( 'NONE',  ( -1.000000000000000000, -0.000000000000000000, -0.000000000000000000 ) ) ;
#4079=DIRECTION ( 'NONE',  ( 1.000000000000000000, 0.000000000000000000, -0.000000000000000000 ) ) ;
#4117=ORIENTED_EDGE ( 'NONE', *, *, #8525, .F. ) ;
#4119=DIRECTION ( 'NONE',  ( -0.000000000000000000, 0.000000000000000000, -1.000000000000000000 ) ) ;
#4141=ORIENTED_EDGE ( 'NONE', *, *, #11691, .F. ) ;
#4164=CARTESIAN_POINT ( 'NONE',  ( 1.040000000000000036, 0.000000000000000000, -1.000000000000000000 ) ) ;
#4176=EDGE_LOOP ( 'NONE', ( #7446, #10998, #5054, #11861, #746 ) ) ;
#4180=AXIS2_PLACEMENT_3D ( 'NONE', #12183, #2375, #8067 ) ;
#4203=DIRECTION ( 'NONE',  ( 0.000000000000000000, 0.000000000000000000, 1.000000000000000000 ) ) ;
#4209=FACE_OUTER_BOUND ( 'NONE', #5639, .T. ) ;
#4220=AXIS2_PLACEMENT_3D ( 'NONE', #9224, #380, #247 ) ;
#4237=DIRECTION ( 'NONE',  ( 0.000000000000000000, 0.000000000000000000, 1.000000000000000000 ) ) ;
#4245=AXIS2_PLACEMENT_3D ( 'NONE', #12290, #2351, #7253 ) ;
#4279=VECTOR ( 'NONE', #7353, 1000.000000000000000 ) ;
#4280=CARTESIAN_POINT ( 'NONE',  ( 7.650000000000000355, 0.000000000000000000, 0.000000000000000000 ) ) ;
#4297=CIRCLE ( 'NONE', #8265, 1.000000000000000000 ) ;
#4327=CARTESIAN_POINT ( 'NONE',  ( 1.040000000000000036, 0.5773502691896263972, 1.000000000000000000 ) ) ;
#4336=PLANE ( 'NONE',  #4180 ) ;
#4388=CARTESIAN_POINT ( 'NONE',  ( 1.649999999999999911, 0.000000000000000000, 1.599999999999999645 ) ) ;
#4391=LINE ( 'NONE', #8186, #6923 ) ;
#4444=ORIENTED_EDGE ( 'NONE', *, *, #1831, .T. ) ;
#4536=ADVANCED_FACE ( 'NONE', ( #1878 ), #9851, .T. ) ;
#4541=CARTESIAN_POINT ( 'NONE',  ( 7.650000000000000355, 0.000000000000000000, 1.219500000000000028 ) ) ;
#4556=CARTESIAN_POINT ( 'NONE',  ( 1.040000000000000036, 1.154700538379252350, -1.084202172485497162E-16 ) ) ;
#4565=ORIENTED_EDGE ( 'NONE', *, *, #7521, .F. ) ;
#4586=ORIENTED_EDGE ( 'NONE', *, *, #7865, .F. ) ;
#4642=EDGE_LOOP ( 'NONE', ( #8885, #2588, #12089 ) ) ;
#4646=ORIENTED_EDGE ( 'NONE', *, *, #9208, .T. ) ;
#4668=DIRECTION ( 'NONE',  ( -1.000000000000000000, 0.000000000000000000, 0.000000000000000000 ) ) ;
#4670=ADVANCED_FACE ( 'NONE', ( #6841 ), #12075, .T. ) ;
#4677=CARTESIAN_POINT ( 'NONE',  ( 1.750000000000000000, 1.836970198721029441E-16, -1.499999999999999556 ) ) ;
#4683=ORIENTED_EDGE ( 'NONE', *, *, #11546, .F. ) ;
#4728=VERTEX_POINT ( 'NONE', #10106 ) ;
#4751=CARTESIAN_POINT ( 'NONE',  ( 1.040000000000000036, 0.000000000000000000, 0.000000000000000000 ) ) ;
#4755=CARTESIAN_POINT ( 'NONE',  ( 0.000000000000000000, 0.5773502691896263972, -1.000000000000000000 ) ) ;
#4762=CARTESIAN_POINT ( 'NONE',  ( 0.000000000000000000, 0.000000000000000000, 0.000000000000000000 ) ) ;
#4782=CARTESIAN_POINT ( 'NONE',  ( 1.040000000000000036, -1.154700538379251684, -1.199226976249124676E-17 ) ) ;
#4785=ADVANCED_FACE ( 'NONE', ( #150 ), #87, .F. ) ;
#4815=CARTESIAN_POINT ( 'NONE',  ( 1.750000000000000000, 0.000000000000000000, 1.599999999999999645 ) ) ;
#4824=DIRECTION ( 'NONE',  ( 0.000000000000000000, 0.000000000000000000, 1.000000000000000000 ) ) ;
#4830=LINE ( 'NONE', #11888, #5723 ) ;
#4832=ORIENTED_EDGE ( 'NONE', *, *, #5394, .F. ) ;
#4846=ORIENTED_EDGE ( 'NONE', *, *, #2587, .F. ) ;
#4854=LINE ( 'NONE', #2105, #12576 ) ;
#4885=CIRCLE ( 'NONE', #3645, 2.849999999999999645 ) ;
#4886=DIRECTION ( 'NONE',  ( 1.000000000000000000, 0.000000000000000000, 0.000000000000000000 ) ) ;
#4890=DIRECTION ( 'NONE',  ( -0.000000000000000000, 0.5000000000000000000, 0.8660254037844385966 ) ) ;
#4913=AXIS2_PLACEMENT_3D ( 'NONE', #12406, #11293, #225 ) ;
#4921=VECTOR ( 'NONE', #5519, 1000.000000000000114 ) ;
#4952=CARTESIAN_POINT ( 'NONE',  ( 1.040000000000000036, 1.154700538379252350, -1.084202172485497162E-16 ) ) ;
#4960=ADVANCED_FACE ( 'NONE', ( #10499 ), #2466, .T. ) ;
#4964=LINE ( 'NONE', #5819, #11751 ) ;
#4967=VECTOR ( 'NONE', #4668, 1000.000000000000000 ) ;
#4969=CARTESIAN_POINT ( 'NONE',  ( 1.040000000000000036, 0.000000000000000000, 0.000000000000000000 ) ) ;
#4997=AXIS2_PLACEMENT_3D ( 'NONE', #5043, #2045, #5174 ) ;
#5001=CARTESIAN_POINT ( 'NONE',  ( 1.040000000000000036, 0.000000000000000000, 1.000000000000000000 ) ) ;
#5014=DIRECTION ( 'NONE',  ( -1.000000000000000000, -0.000000000000000000, -0.000000000000000000 ) ) ;
#5032=VERTEX_POINT ( 'NONE', #2786 ) ;
#5035=CONICAL_SURFACE ( 'NONE', #9219, 1732.050807568857181, 1.047197551196592746 ) ;
#5040=CARTESIAN_POINT ( 'NONE',  ( 0.000000000000000000, 3.490243377569956061E-16, -2.849999999999999645 ) ) ;
#5043=CARTESIAN_POINT ( 'NONE',  ( 1.040000000000000036, 0.5773502691896263972, -1.000000000000000000 ) ) ;
#5054=ORIENTED_EDGE ( 'NONE', *, *, #8525, .T. ) ;
#5081=ORIENTED_EDGE ( 'NONE', *, *, #149, .F. ) ;
#5102=AXIS2_PLACEMENT_3D ( 'NONE', #11604, #10363, #1396 ) ;
#5117=PLANE ( 'NONE',  #5657 ) ;
#5129=CIRCLE ( 'NONE', #8486, 3.351416843938785028 ) ;
#5135=ORIENTED_EDGE ( 'NONE', *, *, #12357, .T. ) ;
#5150=TOROIDAL_SURFACE ( 'NONE', #10587, 1.599999999999999645, 0.1000000000000000056 ) ;
#5153=FACE_OUTER_BOUND ( 'NONE', #5959, .T. ) ;
#5174=DIRECTION ( 'NONE',  ( 1.000000000000000000, 0.000000000000000000, -0.000000000000000000 ) ) ;
#5223=EDGE_CURVE ( 'NONE', #242, #4728, #2263, .T. ) ;
#5226=ORIENTED_EDGE ( 'NONE', *, *, #12643, .T. ) ;
#5243=DIRECTION ( 'NONE',  ( 0.000000000000000000, 0.000000000000000000, 1.000000000000000000 ) ) ;
#5250=CARTESIAN_POINT ( 'NONE',  ( 7.369500000000001272, 0.000000000000000000, 0.000000000000000000 ) ) ;
#5257=DIRECTION ( 'NONE',  ( 0.000000000000000000, 0.000000000000000000, 1.000000000000000000 ) ) ;
#5306=DIRECTION ( 'NONE',  ( -1.000000000000000000, -0.000000000000000000, -0.000000000000000000 ) ) ;
#5308=EDGE_CURVE ( 'NONE', #977, #11518, #9373, .T. ) ;
#5347=EDGE_CURVE ( 'NONE', #261, #7067, #8111, .T. ) ;
#5349=DIRECTION ( 'NONE',  ( -0.000000000000000000, 0.5000000000000000000, 0.8660254037844385966 ) ) ;
#5367=ORIENTED_EDGE ( 'NONE', *, *, #10046, .T. ) ;
#5382=CARTESIAN_POINT ( 'NONE',  ( 1.269999999999999796, -2.850000000000000533, -3.490243377569956061E-16 ) ) ;
#5394=EDGE_CURVE ( 'NONE', #10844, #11492, #5807, .T. ) ;
#5408=VECTOR ( 'NONE', #11600, 1000.000000000000000 ) ;
#5439=DIRECTION ( 'NONE',  ( 1.000000000000000000, 0.000000000000000000, -0.000000000000000000 ) ) ;
#5450=CARTESIAN_POINT ( 'NONE',  ( 1.040000000000000036, 0.000000000000000000, 0.000000000000000000 ) ) ;
#5468=PRESENTATION_STYLE_ASSIGNMENT (( #2476 ) ) ;
#5472=CIRCLE ( 'NONE', #12165, 1.599999999999999645 ) ;
#5474=ORIENTED_EDGE ( 'NONE', *, *, #10364, .T. ) ;
#5478=PLANE ( 'NONE',  #270 ) ;
#5481=EDGE_LOOP ( 'NONE', ( #4646, #3553, #5659, #1433 ) ) ;
#5519=DIRECTION ( 'NONE',  ( -0.000000000000000000, 0.5000000000000003331, -0.8660254037844383745 ) ) ;
#5543=DIRECTION ( 'NONE',  ( -1.000000000000000000, -0.000000000000000000, -0.000000000000000000 ) ) ;
#5546=VECTOR ( 'NONE', #11033, 1000.000000000000000 ) ;
#5561=VERTEX_POINT ( 'NONE', #10409 ) ;
#5639=EDGE_LOOP ( 'NONE', ( #12167, #4141, #224 ) ) ;
#5657=AXIS2_PLACEMENT_3D ( 'NONE', #8978, #12125, #6890 ) ;
#5659=ORIENTED_EDGE ( 'NONE', *, *, #5394, .T. ) ;
#5689=DIRECTION ( 'NONE',  ( 0.000000000000000000, 0.8660254037844384856, -0.5000000000000004441 ) ) ;
#5704=AXIS2_PLACEMENT_3D ( 'NONE', #8997, #4824, #4886 ) ;
#5723=VECTOR ( 'NONE', #2934, 1000.000000000000227 ) ;
#5754=ORIENTED_EDGE ( 'NONE', *, *, #1016, .T. ) ;
#5787=ADVANCED_FACE ( 'NONE', ( #7056 ), #6004, .F. ) ;
#5796=EDGE_LOOP ( 'NONE', ( #2363, #8732, #3783, #2295, #11219 ) ) ;
#5797=EDGE_CURVE ( 'NONE', #10652, #8374, #6130, .T. ) ;
#5807=CIRCLE ( 'NONE', #1416, 1.499999999999999556 ) ;
#5819=CARTESIAN_POINT ( 'NONE',  ( 0.000000000000000000, 1.836970198721029441E-16, -1.499999999999999556 ) ) ;
#5823=CARTESIAN_POINT ( 'NONE',  ( 1.750000000000000000, 0.000000000000000000, 0.000000000000000000 ) ) ;
#5858=CARTESIAN_POINT ( 'NONE',  ( 0.000000000000000000, 0.5773502691896263972, 1.000000000000000000 ) ) ;
#5868=ORIENTED_EDGE ( 'NONE', *, *, #3206, .T. ) ;
#5888=DIRECTION ( 'NONE',  ( -1.000000000000000000, -0.000000000000000000, -0.000000000000000000 ) ) ;
#5917=DIRECTION ( 'NONE',  ( 0.000000000000000000, 0.000000000000000000, -1.000000000000000000 ) ) ;
#5922=MECHANICAL_DESIGN_GEOMETRIC_PRESENTATION_REPRESENTATION('',(#8444),#4063);
#5944=CARTESIAN_POINT ( 'NONE',  ( 0.000000000000000000, 0.5773502691896263972, 1.000000000000000000 ) ) ;
#5959=EDGE_LOOP ( 'NONE', ( #689, #520 ) ) ;
#5960=VECTOR ( 'NONE', #11485, 1000.000000000000000 ) ;
#6000=ORIENTED_EDGE ( 'NONE', *, *, #5223, .T. ) ;
#6004=PLANE ( 'NONE',  #9584 ) ;
#6012=DIRECTION ( 'NONE',  ( 0.000000000000000000, 0.000000000000000000, 1.000000000000000000 ) ) ;
#6023=ORIENTED_EDGE ( 'NONE', *, *, #11632, .T. ) ;
#6026=EDGE_CURVE ( 'NONE', #261, #9467, #6267, .T. ) ;
#6036=ORIENTED_EDGE ( 'NONE', *, *, #149, .T. ) ;
#6040=LINE ( 'NONE', #10033, #156 ) ;
#6043=EDGE_CURVE ( 'NONE', #9467, #10383, #9405, .T. ) ;
#6066=VERTEX_POINT ( 'NONE', #2483 ) ;
#6080=VECTOR ( 'NONE', #6281, 1000.000000000000227 ) ;
#6087=CARTESIAN_POINT ( 'NONE',  ( 1.040000000000000036, 0.8660254037844390407, -0.5000000000000002220 ) ) ;
#6127=EDGE_CURVE ( 'NONE', #5561, #10542, #6040, .T. ) ;
#6130=LINE ( 'NONE', #3208, #12919 ) ;
#6142=ORIENTED_EDGE ( 'NONE', *, *, #10903, .F. ) ;
#6143=DIRECTION ( 'NONE',  ( -0.000000000000000000, -1.000000000000000000, -0.000000000000000000 ) ) ;
#6144=AXIS2_PLACEMENT_3D ( 'NONE', #10933, #1985, #8848 ) ;
#6170=APPLICATION_CONTEXT ( 'automotive_design' ) ;
#6197=ADVANCED_FACE ( 'NONE', ( #8747 ), #11565, .T. ) ;
#6226=VERTEX_POINT ( 'NONE', #2061 ) ;
#6248=DIRECTION ( 'NONE',  ( 0.000000000000000000, 0.000000000000000000, -1.000000000000000000 ) ) ;
#6265=ORIENTED_EDGE ( 'NONE', *, *, #2587, .T. ) ;
#6267=LINE ( 'NONE', #11366, #7697 ) ;
#6273=CARTESIAN_POINT ( 'NONE',  ( 0.000000000000000000, -0.5773502691896253980, -1.000000000000000000 ) ) ;
#6281=DIRECTION ( 'NONE',  ( -0.000000000000000000, -0.5000000000000000000, 0.8660254037844385966 ) ) ;
#6290=FACE_OUTER_BOUND ( 'NONE', #3955, .T. ) ;
#6311=CARTESIAN_POINT ( 'NONE',  ( 1.040000000000000036, -1.154700538379251684, 0.000000000000000000 ) ) ;
#6333=AXIS2_PLACEMENT_3D ( 'NONE', #243, #1040, #1105 ) ;
#6341=DIRECTION ( 'NONE',  ( 0.000000000000000000, -0.8660254037844387076, -0.5000000000000001110 ) ) ;
#6388=FILL_AREA_STYLE_COLOUR ( '', #3434 ) ;
#6433=LINE ( 'NONE', #1599, #4921 ) ;
#6507=MECHANICAL_DESIGN_GEOMETRIC_PRESENTATION_REPRESENTATION('',(#12157),#11731);
#6541=CIRCLE ( 'NONE', #9050, 1.499999999999999778 ) ;
#6581=CARTESIAN_POINT ( 'NONE',  ( 7.650000000000000355, 1.665213485140613626E-16, -1.219500000000000028 ) ) ;
#6585=VERTEX_POINT ( 'NONE', #4388 ) ;
#6593=ORIENTED_EDGE ( 'NONE', *, *, #2400, .F. ) ;
#6608=ORIENTED_EDGE ( 'NONE', *, *, #6993, .T. ) ;
#6660=LINE ( 'NONE', #702, #3772 ) ;
#6665=VECTOR ( 'NONE', #10560, 999.9999999999998863 ) ;
#6679=ORIENTED_EDGE ( 'NONE', *, *, #1016, .F. ) ;
#6714=EDGE_CURVE ( 'NONE', #11446, #3791, #9509, .T. ) ;
#6737=EDGE_LOOP ( 'NONE', ( #12829, #6265, #7534, #8261 ) ) ;
#6752=EDGE_CURVE ( 'NONE', #7727, #977, #12457, .T. ) ;
#6756=DIRECTION ( 'NONE',  ( -1.000000000000000000, -0.000000000000000000, -0.000000000000000000 ) ) ;
#6770=CARTESIAN_POINT ( 'NONE',  ( 0.000000000000000000, -1.154700538379251684, -1.199226976249124676E-17 ) ) ;
#6815=DIRECTION ( 'NONE',  ( 0.000000000000000000, 0.000000000000000000, 1.000000000000000000 ) ) ;
#6818=DIRECTION ( 'NONE',  ( -0.000000000000000000, -1.000000000000000000, -0.000000000000000000 ) ) ;
#6841=FACE_OUTER_BOUND ( 'NONE', #2303, .T. ) ;
#6848=CIRCLE ( 'NONE', #3737, 1.000000000000000000 ) ;
#6849=DIRECTION ( 'NONE',  ( 0.000000000000000000, 0.000000000000000000, 1.000000000000000000 ) ) ;
#6850=AXIS2_PLACEMENT_3D ( 'NONE', #529, #1589, #8465 ) ;
#6852=EDGE_LOOP ( 'NONE', ( #9820, #6608, #10510, #4846 ) ) ;
#6865=FACE_OUTER_BOUND ( 'NONE', #9873, .T. ) ;
#6880=CIRCLE ( 'NONE', #1239, 1.219500000000000028 ) ;
#6885=CARTESIAN_POINT ( 'NONE',  ( 1.649999999999999911, 0.000000000000000000, 0.000000000000000000 ) ) ;
#6890=DIRECTION ( 'NONE',  ( -0.000000000000000000, 0.000000000000000000, -1.000000000000000000 ) ) ;
#6895=DIRECTION ( 'NONE',  ( 0.000000000000000000, 0.000000000000000000, 1.000000000000000000 ) ) ;
#6910=DIRECTION ( 'NONE',  ( 0.000000000000000000, -0.8660254037844387076, 0.5000000000000001110 ) ) ;
#6919=ORIENTED_EDGE ( 'NONE', *, *, #5347, .T. ) ;
#6921=EDGE_CURVE ( 'NONE', #242, #8640, #7717, .T. ) ;
#6923=VECTOR ( 'NONE', #6143, 1000.000000000000000 ) ;
#6978=ORIENTED_EDGE ( 'NONE', *, *, #12357, .F. ) ;
#6981=CARTESIAN_POINT ( 'NONE',  ( 1.040000000000000036, 0.5773502691896263972, -1.000000000000000000 ) ) ;
#6993=EDGE_CURVE ( 'NONE', #10328, #11446, #6880, .T. ) ;
#7001=EDGE_LOOP ( 'NONE', ( #1122, #3404, #7125 ) ) ;
#7011=ADVANCED_FACE ( 'NONE', ( #12049 ), #9230, .T. ) ;
#7056=FACE_OUTER_BOUND ( 'NONE', #441, .T. ) ;
#7067=VERTEX_POINT ( 'NONE', #6087 ) ;
#7117=ORIENTED_EDGE ( 'NONE', *, *, #2719, .T. ) ;
#7123=ORIENTED_EDGE ( 'NONE', *, *, #12869, .F. ) ;
#7125=ORIENTED_EDGE ( 'NONE', *, *, #5797, .F. ) ;
#7145=ORIENTED_EDGE ( 'NONE', *, *, #9208, .F. ) ;
#7147=ORIENTED_EDGE ( 'NONE', *, *, #8348, .F. ) ;
#7200=EDGE_CURVE ( 'NONE', #7727, #261, #6848, .T. ) ;
#7208=CARTESIAN_POINT ( 'NONE',  ( 7.650000000000000355, 0.000000000000000000, 0.000000000000000000 ) ) ;
#7215=CIRCLE ( 'NONE', #3255, 2.849999999999999645 ) ;
#7233=EDGE_CURVE ( 'NONE', #8374, #12039, #12621, .T. ) ;
#7234=CARTESIAN_POINT ( 'NONE',  ( 1.040000000000000036, -0.8660254037844382635, 0.5000000000000002220 ) ) ;
#7239=ADVANCED_FACE ( 'NONE', ( #2991 ), #3850, .T. ) ;
#7253=DIRECTION ( 'NONE',  ( -0.000000000000000000, 0.000000000000000000, 1.000000000000000000 ) ) ;
#7277=CARTESIAN_POINT ( 'NONE',  ( 1.040000000000000036, -1.154700538379251684, 0.000000000000000000 ) ) ;
#7280=DIRECTION ( 'NONE',  ( -1.000000000000000000, -0.000000000000000000, -0.000000000000000000 ) ) ;
#7289=CARTESIAN_POINT ( 'NONE',  ( 1.040000000000000036, 0.5773502691896263972, -1.000000000000000000 ) ) ;
#7298=ORIENTED_EDGE ( 'NONE', *, *, #2248, .T. ) ;
#7328=ORIENTED_EDGE ( 'NONE', *, *, #2086, .F. ) ;
#7340=PLANE ( 'NONE',  #11266 ) ;
#7350=CARTESIAN_POINT ( 'NONE',  ( 1.040000000000000036, -0.5773502691896253980, 1.000000000000000000 ) ) ;
#7352=CARTESIAN_POINT ( 'NONE',  ( 1.040000000000000036, -0.5773502691896253980, 1.000000000000000000 ) ) ;
#7353=DIRECTION ( 'NONE',  ( -0.000000000000000000, 1.000000000000000000, -0.000000000000000000 ) ) ;
#7393=CARTESIAN_POINT ( 'NONE',  ( 1.040000000000000036, 0.5773502691896263972, 1.000000000000000000 ) ) ;
#7415=CIRCLE ( 'NONE', #8468, 1.000000000000000000 ) ;
#7446=ORIENTED_EDGE ( 'NONE', *, *, #9188, .F. ) ;
#7448=CARTESIAN_POINT ( 'NONE',  ( 0.000000000000000000, 0.000000000000000000, 2.849999999999999645 ) ) ;
#7469=EDGE_LOOP ( 'NONE', ( #2929, #909, #12753, #7147, #8958 ) ) ;
#7521=EDGE_CURVE ( 'NONE', #4728, #6066, #2813, .T. ) ;
#7534=ORIENTED_EDGE ( 'NONE', *, *, #9842, .T. ) ;
#7576=CARTESIAN_POINT ( 'NONE',  ( 0.000000000000000000, -0.5773502691896253980, -1.000000000000000000 ) ) ;
#7616=CARTESIAN_POINT ( 'NONE',  ( 0.000000000000000000, 0.000000000000000000, 0.000000000000000000 ) ) ;
#7624=VECTOR ( 'NONE', #6818, 1000.000000000000000 ) ;
#7642=CIRCLE ( 'NONE', #10139, 2.849999999999999645 ) ;
#7683=APPLICATION_CONTEXT ( 'automotive_design' ) ;
#7697=VECTOR ( 'NONE', #2417, 1000.000000000000227 ) ;
#7704=DIRECTION ( 'NONE',  ( 0.000000000000000000, 0.000000000000000000, 1.000000000000000000 ) ) ;
#7713=CARTESIAN_POINT ( 'NONE',  ( 1.040000000000000036, -0.8660254037844384856, -0.5000000000000003331 ) ) ;
#7715=CIRCLE ( 'NONE', #9804, 1.499999999999999556 ) ;
#7717=CIRCLE ( 'NONE', #3125, 2.849999999999999645 ) ;
#7726=LINE ( 'NONE', #5944, #12437 ) ;
#7727=VERTEX_POINT ( 'NONE', #5001 ) ;
#7758=EDGE_CURVE ( 'NONE', #11518, #12039, #2063, .T. ) ;
#7799=CARTESIAN_POINT ( 'NONE',  ( 1.269999999999999796, 0.000000000000000000, 0.000000000000000000 ) ) ;
#7836=CARTESIAN_POINT ( 'NONE',  ( 2.168404344971008868E-16, 0.000000000000000000, 0.000000000000000000 ) ) ;
#7865=EDGE_CURVE ( 'NONE', #10542, #2484, #11077, .T. ) ;
#7867=ORIENTED_EDGE ( 'NONE', *, *, #9188, .T. ) ;
#7872=EDGE_LOOP ( 'NONE', ( #10732, #3233, #4586 ) ) ;
#7873=CARTESIAN_POINT ( 'NONE',  ( 1.649999999999999911, 0.000000000000000000, 0.000000000000000000 ) ) ;
#7877=FACE_OUTER_BOUND ( 'NONE', #7872, .T. ) ;
#7894=ORIENTED_EDGE ( 'NONE', *, *, #6127, .T. ) ;
#7921=VERTEX_POINT ( 'NONE', #2264 ) ;
#7936=CARTESIAN_POINT ( 'NONE',  ( 7.369500000000001272, 0.000000000000000000, 0.000000000000000000 ) ) ;
#7938=VERTEX_POINT ( 'NONE', #5382 ) ;
#7954=AXIS2_PLACEMENT_3D ( 'NONE', #4280, #8268, #11267 ) ;
#7961=ADVANCED_FACE ( 'NONE', ( #9576 ), #12386, .T. ) ;
#7987=ORIENTED_EDGE ( 'NONE', *, *, #12794, .F. ) ;
#8067=DIRECTION ( 'NONE',  ( -0.000000000000000000, 0.000000000000000000, 1.000000000000000000 ) ) ;
#8111=CIRCLE ( 'NONE', #6850, 1.000000000000000000 ) ;
#8122=DIRECTION ( 'NONE',  ( -1.000000000000000000, -0.000000000000000000, -0.000000000000000000 ) ) ;
#8172=VECTOR ( 'NONE', #10627, 1000.000000000000114 ) ;
#8186=CARTESIAN_POINT ( 'NONE',  ( 1.040000000000000036, -0.5773502691896253980, 1.000000000000000000 ) ) ;
#8208=VECTOR ( 'NONE', #5543, 1000.000000000000000 ) ;
#8217=DIRECTION ( 'NONE',  ( -0.000000000000000000, 0.000000000000000000, -1.000000000000000000 ) ) ;
#8245=PRODUCT_CONTEXT ( 'NONE', #6170, 'mechanical' ) ;
#8251=CARTESIAN_POINT ( 'NONE',  ( 1.649999999999999911, 0.000000000000000000, 0.000000000000000000 ) ) ;
#8261=ORIENTED_EDGE ( 'NONE', *, *, #8949, .T. ) ;
#8265=AXIS2_PLACEMENT_3D ( 'NONE', #4969, #12232, #2097 ) ;
#8268=DIRECTION ( 'NONE',  ( -1.000000000000000000, -0.000000000000000000, -0.000000000000000000 ) ) ;
#8278=CIRCLE ( 'NONE', #2646, 2.849999999999999645 ) ;
#8281=CARTESIAN_POINT ( 'NONE',  ( 1.750000000000000000, 1.959434878635764737E-16, -1.599999999999999645 ) ) ;
#8303=ADVANCED_FACE ( 'NONE', ( #6865 ), #2196, .F. ) ;
#8318=AXIS2_PLACEMENT_3D ( 'NONE', #1263, #5257, #9244 ) ;
#8322=ORIENTED_EDGE ( 'NONE', *, *, #10709, .F. ) ;
#8327=CARTESIAN_POINT ( 'NONE',  ( 1.040000000000000036, 0.5773502691896263972, 1.000000000000000000 ) ) ;
#8331=FACE_OUTER_BOUND ( 'NONE', #7001, .T. ) ;
#8348=EDGE_CURVE ( 'NONE', #6226, #10383, #7726, .T. ) ;
#8350=DIRECTION ( 'NONE',  ( 0.000000000000000000, 1.000000000000000000, 0.000000000000000000 ) ) ;
#8374=VERTEX_POINT ( 'NONE', #4782 ) ;
#8424=( NAMED_UNIT ( * ) PLANE_ANGLE_UNIT ( ) SI_UNIT ( $, .RADIAN. ) );
#8444=STYLED_ITEM ( 'NONE', ( #5468 ), #10270 ) ;
#8451=AXIS2_PLACEMENT_3D ( 'NONE', #10178, #1214, #4237 ) ;
#8465=DIRECTION ( 'NONE',  ( 0.000000000000000000, 0.000000000000000000, 1.000000000000000000 ) ) ;
#8468=AXIS2_PLACEMENT_3D ( 'NONE', #5450, #2778, #1856 ) ;
#8486=AXIS2_PLACEMENT_3D ( 'NONE', #538, #2584, #3636 ) ;
#8509=ORIENTED_EDGE ( 'NONE', *, *, #8758, .F. ) ;
#8523=DIRECTION ( 'NONE',  ( -0.000000000000000000, 0.000000000000000000, -1.000000000000000000 ) ) ;
#8524=VERTEX_POINT ( 'NONE', #6273 ) ;
#8525=EDGE_CURVE ( 'NONE', #10542, #9930, #4297, .T. ) ;
#8544=FACE_OUTER_BOUND ( 'NONE', #12375, .T. ) ;
#8564=EDGE_LOOP ( 'NONE', ( #7894, #3446, #5367, #11394, #1384 ) ) ;
#8628=DIRECTION ( 'NONE',  ( -1.000000000000000000, -0.000000000000000000, -0.000000000000000000 ) ) ;
#8636=DIRECTION ( 'NONE',  ( 0.000000000000000000, 0.5000000000000003331, 0.8660254037844383745 ) ) ;
#8640=VERTEX_POINT ( 'NONE', #11437 ) ;
#8708=DIRECTION ( 'NONE',  ( 0.000000000000000000, 0.000000000000000000, 1.000000000000000000 ) ) ;
#8732=ORIENTED_EDGE ( 'NONE', *, *, #6752, .T. ) ;
#8747=FACE_OUTER_BOUND ( 'NONE', #9421, .T. ) ;
#8758=EDGE_CURVE ( 'NONE', #8640, #7938, #7215, .T. ) ;
#8772=EDGE_LOOP ( 'NONE', ( #5226, #12094, #5868, #5081, #10339 ) ) ;
#8782=CARTESIAN_POINT ( 'NONE',  ( 1.269999999999999796, 0.000000000000000000, 0.000000000000000000 ) ) ;
#8783=ADVANCED_FACE ( 'NONE', ( #9798, #12685 ), #766, .T. ) ;
#8795=( NAMED_UNIT ( * ) PLANE_ANGLE_UNIT ( ) SI_UNIT ( $, .RADIAN. ) );
#8801=CIRCLE ( 'NONE', #3176, 1.599999999999999645 ) ;
#8806=ORIENTED_EDGE ( 'NONE', *, *, #34, .T. ) ;
#8810=DIRECTION ( 'NONE',  ( -0.000000000000000000, 1.000000000000000000, -0.000000000000000000 ) ) ;
#8845=ORIENTED_EDGE ( 'NONE', *, *, #7758, .T. ) ;
#8848=DIRECTION ( 'NONE',  ( 0.000000000000000000, 0.000000000000000000, 1.000000000000000000 ) ) ;
#8885=ORIENTED_EDGE ( 'NONE', *, *, #5347, .F. ) ;
#8944=ORIENTED_EDGE ( 'NONE', *, *, #3350, .T. ) ;
#8949=EDGE_CURVE ( 'NONE', #11492, #10844, #7715, .T. ) ;
#8950=AXIS2_PLACEMENT_3D ( 'NONE', #4762, #2611, #7704 ) ;
#8958=ORIENTED_EDGE ( 'NONE', *, *, #3206, .F. ) ;
#8973=CARTESIAN_POINT ( 'NONE',  ( 1.617350269189632428, 0.000000000000000000, 0.000000000000000000 ) ) ;
#8978=CARTESIAN_POINT ( 'NONE',  ( 1.040000000000000036, -1.154700538379251684, 0.000000000000000000 ) ) ;
#8997=CARTESIAN_POINT ( 'NONE',  ( 0.000000000000000000, 0.000000000000000000, 0.000000000000000000 ) ) ;
#9028=CARTESIAN_POINT ( 'NONE',  ( -998.3826497308103853, 0.000000000000000000, 0.000000000000000000 ) ) ;
#9050=AXIS2_PLACEMENT_3D ( 'NONE', #5250, #7280, #10084 ) ;
#9090=CIRCLE ( 'NONE', #10134, 0.1000000000000000472 ) ;
#9095=CARTESIAN_POINT ( 'NONE',  ( 7.650000000000000355, 0.000000000000000000, 1.219500000000000028 ) ) ;
#9136=AXIS2_PLACEMENT_3D ( 'NONE', #6311, #9326, #8217 ) ;
#9139=ORIENTED_EDGE ( 'NONE', *, *, #5797, .T. ) ;
#9188=EDGE_CURVE ( 'NONE', #11115, #7727, #10747, .T. ) ;
#9208=EDGE_CURVE ( 'NONE', #3791, #2398, #2736, .T. ) ;
#9219=AXIS2_PLACEMENT_3D ( 'NONE', #9028, #5888, #9881 ) ;
#9224=CARTESIAN_POINT ( 'NONE',  ( 0.000000000000000000, 0.000000000000000000, 0.000000000000000000 ) ) ;
#9230=PLANE ( 'NONE',  #4997 ) ;
#9234=DIRECTION ( 'NONE',  ( -0.000000000000000000, 0.000000000000000000, -1.000000000000000000 ) ) ;
#9244=DIRECTION ( 'NONE',  ( 1.000000000000000000, 0.000000000000000000, 0.000000000000000000 ) ) ;
#9265=CARTESIAN_POINT ( 'NONE',  ( 1.269999999999999796, 2.849999999999999645, 0.000000000000000000 ) ) ;
#9292=PLANE ( 'NONE',  #2962 ) ;
#9294=AXIS2_PLACEMENT_3D ( 'NONE', #5823, #9751, #8708 ) ;
#9326=DIRECTION ( 'NONE',  ( 1.000000000000000000, 0.000000000000000000, -0.000000000000000000 ) ) ;
#9373=LINE ( 'NONE', #7350, #4967 ) ;
#9400=( NAMED_UNIT ( * ) SI_UNIT ( $, .STERADIAN. ) SOLID_ANGLE_UNIT ( ) );
#9405=LINE ( 'NONE', #2547, #10829 ) ;
#9421=EDGE_LOOP ( 'NONE', ( #4683, #3870, #12884, #11677, #8509 ) ) ;
#9422=CARTESIAN_POINT ( 'NONE',  ( 1.649999999999999911, 0.000000000000000000, 0.000000000000000000 ) ) ;
#9427=ADVANCED_FACE ( 'NONE', ( #4209 ), #7340, .F. ) ;
#9442=ADVANCED_FACE ( 'NONE', ( #10080, #6290 ), #4336, .F. ) ;
#9467=VERTEX_POINT ( 'NONE', #8327 ) ;
#9509=LINE ( 'NONE', #4541, #6665 ) ;
#9514=DIRECTION ( 'NONE',  ( -1.000000000000000000, -0.000000000000000000, -0.000000000000000000 ) ) ;
#9516=AXIS2_PLACEMENT_3D ( 'NONE', #7616, #9514, #12659 ) ;
#9523=SHAPE_REPRESENTATION ( 'socket button head screw_iso_ISO 7380 - M3 x 6 - 6N', ( #5704 ), #12825 ) ;
#9576=FACE_OUTER_BOUND ( 'NONE', #10847, .T. ) ;
#9584=AXIS2_PLACEMENT_3D ( 'NONE', #2155, #3995, #4119 ) ;
#9608=EDGE_LOOP ( 'NONE', ( #6142, #7867, #12502, #6919, #475 ) ) ;
#9610=ORIENTED_EDGE ( 'NONE', *, *, #10709, .T. ) ;
#9700=AXIS2_PLACEMENT_3D ( 'NONE', #4751, #874, #937 ) ;
#9704=LINE ( 'NONE', #740, #8172 ) ;
#9721=LINE ( 'NONE', #4755, #11709 ) ;
#9751=DIRECTION ( 'NONE',  ( -1.000000000000000000, -0.000000000000000000, -0.000000000000000000 ) ) ;
#9798=FACE_OUTER_BOUND ( 'NONE', #3863, .T. ) ;
#9804=AXIS2_PLACEMENT_3D ( 'NONE', #402, #1398, #2198 ) ;
#9810=DIRECTION ( 'NONE',  ( -1.000000000000000000, -0.000000000000000000, -0.000000000000000000 ) ) ;
#9820=ORIENTED_EDGE ( 'NONE', *, *, #10364, .F. ) ;
#9822=CARTESIAN_POINT ( 'NONE',  ( 2.168404344971008868E-16, -0.5773502691896253980, 1.000000000000000000 ) ) ;
#9827=DIRECTION ( 'NONE',  ( -1.000000000000000000, -0.000000000000000000, -0.000000000000000000 ) ) ;
#9842=EDGE_CURVE ( 'NONE', #3791, #11492, #6660, .T. ) ;
#9851=SPHERICAL_SURFACE ( 'NONE', #3081, 3.351416843938785028 ) ;
#9865=CARTESIAN_POINT ( 'NONE',  ( 1.040000000000000036, -0.5773502691896253980, -1.000000000000000000 ) ) ;
#9873=EDGE_LOOP ( 'NONE', ( #8322, #6978, #4444, #4832 ) ) ;
#9874=DIRECTION ( 'NONE',  ( -0.000000000000000000, -0.5000000000000000000, 0.8660254037844385966 ) ) ;
#9881=DIRECTION ( 'NONE',  ( 0.000000000000000000, 0.000000000000000000, 1.000000000000000000 ) ) ;
#9914=ORIENTED_EDGE ( 'NONE', *, *, #11632, .F. ) ;
#9930=VERTEX_POINT ( 'NONE', #7713 ) ;
#10026=CARTESIAN_POINT ( 'NONE',  ( 1.040000000000000036, -1.154700538379251684, 0.000000000000000000 ) ) ;
#10033=CARTESIAN_POINT ( 'NONE',  ( 1.040000000000000036, 0.5773502691896263972, -1.000000000000000000 ) ) ;
#10046=EDGE_CURVE ( 'NONE', #2484, #10256, #3198, .T. ) ;
#10076=DIRECTION ( 'NONE',  ( 1.000000000000000000, 0.000000000000000000, 0.000000000000000000 ) ) ;
#10080=FACE_BOUND ( 'NONE', #118, .T. ) ;
#10084=DIRECTION ( 'NONE',  ( 0.000000000000000000, 0.000000000000000000, 1.000000000000000000 ) ) ;
#10106=CARTESIAN_POINT ( 'NONE',  ( 4.336808689942017736E-16, 1.424999999999999822, 0.000000000000000000 ) ) ;
#10134=AXIS2_PLACEMENT_3D ( 'NONE', #4815, #1933, #2001 ) ;
#10139=AXIS2_PLACEMENT_3D ( 'NONE', #7799, #2840, #6815 ) ;
#10174=CARTESIAN_POINT ( 'NONE',  ( 3.033375984251970081, -8.673617379884035472E-16, 0.000000000000000000 ) ) ;
#10178=CARTESIAN_POINT ( 'NONE',  ( 4.336808689942017736E-16, 0.000000000000000000, 0.000000000000000000 ) ) ;
#10256=VERTEX_POINT ( 'NONE', #421 ) ;
#10270=ADVANCED_BREP_SHAPE_REPRESENTATION ( '', ( #12002, #5704 ), #12825 ) ;
#10271=FACE_OUTER_BOUND ( 'NONE', #5481, .T. ) ;
#10316=( LENGTH_UNIT ( ) NAMED_UNIT ( * ) SI_UNIT ( .MILLI., .METRE. ) );
#10320=EDGE_CURVE ( 'NONE', #8524, #10256, #9721, .T. ) ;
#10325=EDGE_LOOP ( 'NONE', ( #5754, #2053, #1173, #3558, #7987 ) ) ;
#10327=PRODUCT_DEFINITION_SHAPE ( 'NONE', 'NONE',  #3872 ) ;
#10328=VERTEX_POINT ( 'NONE', #6581 ) ;
#10339=ORIENTED_EDGE ( 'NONE', *, *, #10046, .F. ) ;
#10343=DIRECTION ( 'NONE',  ( -1.000000000000000000, -0.000000000000000000, -0.000000000000000000 ) ) ;
#10363=DIRECTION ( 'NONE',  ( 0.000000000000000000, 0.8660254037844384856, 0.5000000000000004441 ) ) ;
#10364=EDGE_CURVE ( 'NONE', #10328, #2398, #1682, .T. ) ;
#10383=VERTEX_POINT ( 'NONE', #5858 ) ;
#10404=LINE ( 'NONE', #7393, #6080 ) ;
#10409=CARTESIAN_POINT ( 'NONE',  ( 1.040000000000000036, -0.5773502691896253980, -1.000000000000000000 ) ) ;
#10449=( NAMED_UNIT ( * ) PLANE_ANGLE_UNIT ( ) SI_UNIT ( $, .RADIAN. ) );
#10458=CIRCLE ( 'NONE', #10871, 0.1000000000000000472 ) ;
#10469=ORIENTED_EDGE ( 'NONE', *, *, #1063, .T. ) ;
#10494=DIRECTION ( 'NONE',  ( 0.000000000000000000, -1.224646799147353207E-16, 1.000000000000000000 ) ) ;
#10499=FACE_OUTER_BOUND ( 'NONE', #755, .T. ) ;
#10510=ORIENTED_EDGE ( 'NONE', *, *, #6714, .T. ) ;
#10523=DIRECTION ( 'NONE',  ( -1.000000000000000000, 0.000000000000000000, -0.000000000000000000 ) ) ;
#10526=CIRCLE ( 'NONE', #2175, 1.000000000000000000 ) ;
#10542=VERTEX_POINT ( 'NONE', #4164 ) ;
#10560=DIRECTION ( 'NONE',  ( -0.7071067811865472397, 0.000000000000000000, 0.7071067811865479058 ) ) ;
#10587=AXIS2_PLACEMENT_3D ( 'NONE', #12532, #11411, #2461 ) ;
#10621=AXIS2_PLACEMENT_3D ( 'NONE', #4952, #6910, #10960 ) ;
#10627=DIRECTION ( 'NONE',  ( -0.5000000000000042188, 1.060575238724903710E-16, -0.8660254037844361541 ) ) ;
#10630=( NAMED_UNIT ( * ) SI_UNIT ( $, .STERADIAN. ) SOLID_ANGLE_UNIT ( ) );
#10652=VERTEX_POINT ( 'NONE', #7234 ) ;
#10656=ORIENTED_EDGE ( 'NONE', *, *, #2248, .F. ) ;
#10709=EDGE_CURVE ( 'NONE', #7921, #10844, #10458, .T. ) ;
#10714=DIRECTION ( 'NONE',  ( -1.000000000000000000, 0.000000000000000000, -0.000000000000000000 ) ) ;
#10732=ORIENTED_EDGE ( 'NONE', *, *, #517, .F. ) ;
#10747=LINE ( 'NONE', #8973, #12306 ) ;
#10788=ADVANCED_FACE ( 'NONE', ( #800 ), #12558, .F. ) ;
#10816=CARTESIAN_POINT ( 'NONE',  ( -998.3826497308103853, 0.000000000000000000, 0.000000000000000000 ) ) ;
#10829=VECTOR ( 'NONE', #12417, 1000.000000000000000 ) ;
#10830=DIRECTION ( 'NONE',  ( -0.7071067811865472397, 8.659560562354937789E-17, -0.7071067811865479058 ) ) ;
#10834=ORIENTED_EDGE ( 'NONE', *, *, #2311, .T. ) ;
#10844=VERTEX_POINT ( 'NONE', #4677 ) ;
#10847=EDGE_LOOP ( 'NONE', ( #1259, #10834, #8944, #7123, #1900 ) ) ;
#10855=ORIENTED_EDGE ( 'NONE', *, *, #7521, .T. ) ;
#10871=AXIS2_PLACEMENT_3D ( 'NONE', #8281, #11474, #10494 ) ;
#10887=VECTOR ( 'NONE', #1907, 1000.000000000000000 ) ;
#10903=EDGE_CURVE ( 'NONE', #11115, #10542, #9704, .T. ) ;
#10911=DIRECTION ( 'NONE',  ( -0.000000000000000000, -0.5000000000000003331, -0.8660254037844383745 ) ) ;
#10932=DIRECTION ( 'NONE',  ( 0.000000000000000000, 0.000000000000000000, 1.000000000000000000 ) ) ;
#10933=CARTESIAN_POINT ( 'NONE',  ( 7.650000000000000355, 0.000000000000000000, 0.000000000000000000 ) ) ;
#10937=ORIENTED_EDGE ( 'NONE', *, *, #6127, .F. ) ;
#10960=DIRECTION ( 'NONE',  ( 0.000000000000000000, -0.5000000000000000000, -0.8660254037844385966 ) ) ;
#10972=EDGE_LOOP ( 'NONE', ( #4117, #10937, #775 ) ) ;
#10976=ADVANCED_FACE ( 'NONE', ( #7877 ), #5117, .F. ) ;
#10998=ORIENTED_EDGE ( 'NONE', *, *, #10903, .T. ) ;
#11029=ORIENTED_EDGE ( 'NONE', *, *, #1831, .F. ) ;
#11033=DIRECTION ( 'NONE',  ( -1.000000000000000000, 0.000000000000000000, 0.000000000000000000 ) ) ;
#11034=ORIENTED_EDGE ( 'NONE', *, *, #8348, .T. ) ;
#11077=LINE ( 'NONE', #7289, #4279 ) ;
#11115=VERTEX_POINT ( 'NONE', #1192 ) ;
#11132=UNCERTAINTY_MEASURE_WITH_UNIT (LENGTH_MEASURE( 1.000000000000000082E-05 ), #10316, 'distance_accuracy_value', 'NONE');
#11144=DIRECTION ( 'NONE',  ( -0.000000000000000000, -0.5000000000000003331, -0.8660254037844383745 ) ) ;
#11199=ORIENTED_EDGE ( 'NONE', *, *, #6714, .F. ) ;
#11219=ORIENTED_EDGE ( 'NONE', *, *, #6043, .F. ) ;
#11247=ADVANCED_FACE ( 'NONE', ( #262 ), #12138, .T. ) ;
#11266=AXIS2_PLACEMENT_3D ( 'NONE', #7277, #4079, #9234 ) ;
#11267=DIRECTION ( 'NONE',  ( 0.000000000000000000, 0.000000000000000000, 1.000000000000000000 ) ) ;
#11293=DIRECTION ( 'NONE',  ( 1.000000000000000000, 0.000000000000000000, -0.000000000000000000 ) ) ;
#11352=LINE ( 'NONE', #4556, #5960 ) ;
#11357=FACE_OUTER_BOUND ( 'NONE', #4642, .T. ) ;
#11366=CARTESIAN_POINT ( 'NONE',  ( 1.040000000000000036, 0.5773502691896263972, 1.000000000000000000 ) ) ;
#11375=ORIENTED_EDGE ( 'NONE', *, *, #6921, .T. ) ;
#11379=CYLINDRICAL_SURFACE ( 'NONE', #4220, 1.499999999999999556 ) ;
#11387=ORIENTED_EDGE ( 'NONE', *, *, #2086, .T. ) ;
#11394=ORIENTED_EDGE ( 'NONE', *, *, #10320, .F. ) ;
#11411=DIRECTION ( 'NONE',  ( -1.000000000000000000, -0.000000000000000000, -0.000000000000000000 ) ) ;
#11437=CARTESIAN_POINT ( 'NONE',  ( 1.269999999999999796, 3.490243377569956061E-16, -2.849999999999999645 ) ) ;
#11446=VERTEX_POINT ( 'NONE', #9095 ) ;
#11474=DIRECTION ( 'NONE',  ( -0.000000000000000000, 1.000000000000000000, 1.224646799147353207E-16 ) ) ;
#11485=DIRECTION ( 'NONE',  ( -1.000000000000000000, 0.000000000000000000, 0.000000000000000000 ) ) ;
#11492=VERTEX_POINT ( 'NONE', #850 ) ;
#11518=VERTEX_POINT ( 'NONE', #9822 ) ;
#11539=EDGE_CURVE ( 'NONE', #8374, #9930, #4854, .T. ) ;
#11546=EDGE_CURVE ( 'NONE', #12580, #8640, #3881, .T. ) ;
#11559=ADVANCED_FACE ( 'NONE', ( #910 ), #5035, .F. ) ;
#11564=DIRECTION ( 'NONE',  ( -0.000000000000000000, 0.5000000000000003331, -0.8660254037844383745 ) ) ;
#11565=CYLINDRICAL_SURFACE ( 'NONE', #8950, 2.849999999999999645 ) ;
#11584=EDGE_LOOP ( 'NONE', ( #11375, #1553, #7298, #4565, #278 ) ) ;
#11590=CIRCLE ( 'NONE', #6144, 1.219500000000000028 ) ;
#11600=DIRECTION ( 'NONE',  ( -0.000000000000000000, -1.000000000000000000, -0.000000000000000000 ) ) ;
#11604=CARTESIAN_POINT ( 'NONE',  ( 1.040000000000000036, -0.5773502691896253980, -1.000000000000000000 ) ) ;
#11621=EDGE_CURVE ( 'NONE', #112, #261, #10404, .T. ) ;
#11632=EDGE_CURVE ( 'NONE', #7921, #6585, #8801, .T. ) ;
#11661=DIRECTION ( 'NONE',  ( 0.000000000000000000, 0.000000000000000000, 1.000000000000000000 ) ) ;
#11672=ADVANCED_FACE ( 'NONE', ( #10271 ), #11379, .T. ) ;
#11677=ORIENTED_EDGE ( 'NONE', *, *, #34, .F. ) ;
#11691=EDGE_CURVE ( 'NONE', #9467, #7727, #4391, .T. ) ;
#11693=DIRECTION ( 'NONE',  ( -1.000000000000000000, 0.000000000000000000, 0.000000000000000000 ) ) ;
#11695=DIRECTION ( 'NONE',  ( 0.000000000000000000, 0.000000000000000000, -1.000000000000000000 ) ) ;
#11709=VECTOR ( 'NONE', #3652, 1000.000000000000000 ) ;
#11712=ADVANCED_FACE ( 'NONE', ( #1306 ), #9292, .T. ) ;
#11714=EDGE_LOOP ( 'NONE', ( #11387, #9139, #3491, #2098, #2703 ) ) ;
#11731=( GEOMETRIC_REPRESENTATION_CONTEXT ( 3 ) GLOBAL_UNCERTAINTY_ASSIGNED_CONTEXT ( ( #2696 ) ) GLOBAL_UNIT_ASSIGNED_CONTEXT ( ( #163, #8795, #10630 ) ) REPRESENTATION_CONTEXT ( 'NONE', 'WORKASPACE' ) );
#11737=CARTESIAN_POINT ( 'NONE',  ( 7.650000000000000355, 0.000000000000000000, 0.000000000000000000 ) ) ;
#11751=VECTOR ( 'NONE', #9810, 1000.000000000000000 ) ;
#11762=VERTEX_POINT ( 'NONE', #1763 ) ;
#11861=ORIENTED_EDGE ( 'NONE', *, *, #81, .T. ) ;
#11888=CARTESIAN_POINT ( 'NONE',  ( 0.000000000000000000, 1.154700538379252350, -1.084202172485497162E-16 ) ) ;
#11922=DIRECTION ( 'NONE',  ( -1.000000000000000000, -0.000000000000000000, -0.000000000000000000 ) ) ;
#11941=CARTESIAN_POINT ( 'NONE',  ( 3.033375984251970081, -8.673617379884035472E-16, 0.000000000000000000 ) ) ;
#11947=LINE ( 'NONE', #1944, #3009 ) ;
#12002=MANIFOLD_SOLID_BREP ( 'Hex', #3437 ) ;
#12017=CARTESIAN_POINT ( 'NONE',  ( 1.040000000000000036, 1.154700538379252350, -1.084202172485497162E-16 ) ) ;
#12039=VERTEX_POINT ( 'NONE', #3370 ) ;
#12045=CARTESIAN_POINT ( 'NONE',  ( 1.750000000000000000, 0.000000000000000000, 0.000000000000000000 ) ) ;
#12049=FACE_OUTER_BOUND ( 'NONE', #8564, .T. ) ;
#12075=SPHERICAL_SURFACE ( 'NONE', #12691, 3.351416843938785028 ) ;
#12089=ORIENTED_EDGE ( 'NONE', *, *, #109, .F. ) ;
#12094=ORIENTED_EDGE ( 'NONE', *, *, #109, .T. ) ;
#12125=DIRECTION ( 'NONE',  ( 1.000000000000000000, 0.000000000000000000, -0.000000000000000000 ) ) ;
#12138=CONICAL_SURFACE ( 'NONE', #7954, 1.219500000000000028, 0.7853981633974487231 ) ;
#12140=CARTESIAN_POINT ( 'NONE',  ( 7.369500000000001272, 0.000000000000000000, 1.499999999999999778 ) ) ;
#12157=STYLED_ITEM('',(#13009),#12002);
#12165=AXIS2_PLACEMENT_3D ( 'NONE', #9422, #10343, #2367 ) ;
#12167=ORIENTED_EDGE ( 'NONE', *, *, #7200, .F. ) ;
#12170=CYLINDRICAL_SURFACE ( 'NONE', #1953, 2.849999999999999645 ) ;
#12173=DIRECTION ( 'NONE',  ( 0.000000000000000000, 0.000000000000000000, 1.000000000000000000 ) ) ;
#12183=CARTESIAN_POINT ( 'NONE',  ( 1.649999999999999911, 1.499999999999999112, 0.000000000000000000 ) ) ;
#12232=DIRECTION ( 'NONE',  ( -1.000000000000000000, -0.000000000000000000, -0.000000000000000000 ) ) ;
#12290=CARTESIAN_POINT ( 'NONE',  ( 7.650000000000000355, 0.000000000000000000, 0.000000000000000000 ) ) ;
#12293=ORIENTED_EDGE ( 'NONE', *, *, #10320, .T. ) ;
#12306=VECTOR ( 'NONE', #4017, 1000.000000000000114 ) ;
#12339=AXIS2_PLACEMENT_3D ( 'NONE', #7836, #10714, #887 ) ;
#12357=EDGE_CURVE ( 'NONE', #6585, #7921, #5472, .T. ) ;
#12375=EDGE_LOOP ( 'NONE', ( #9914, #9610, #962, #11029 ) ) ;
#12386=PLANE ( 'NONE',  #5102 ) ;
#12390=AXIS2_PLACEMENT_3D ( 'NONE', #10026, #5439, #8523 ) ;
#12406=CARTESIAN_POINT ( 'NONE',  ( 1.040000000000000036, -1.154700538379251684, 0.000000000000000000 ) ) ;
#12417=DIRECTION ( 'NONE',  ( -1.000000000000000000, 0.000000000000000000, 0.000000000000000000 ) ) ;
#12437=VECTOR ( 'NONE', #9874, 1000.000000000000227 ) ;
#12457=LINE ( 'NONE', #7352, #5408 ) ;
#12491=AXIS2_PLACEMENT_3D ( 'NONE', #11737, #4027, #6895 ) ;
#12502=ORIENTED_EDGE ( 'NONE', *, *, #7200, .T. ) ;
#12532=CARTESIAN_POINT ( 'NONE',  ( 1.750000000000000000, 0.000000000000000000, 0.000000000000000000 ) ) ;
#12550=( NAMED_UNIT ( * ) SI_UNIT ( $, .STERADIAN. ) SOLID_ANGLE_UNIT ( ) );
#12558=CONICAL_SURFACE ( 'NONE', #410, 1732.050807568857181, 1.047197551196592746 ) ;
#12559=DIRECTION ( 'NONE',  ( 0.000000000000000000, 0.000000000000000000, 1.000000000000000000 ) ) ;
#12566=PLANE ( 'NONE',  #105 ) ;
#12576=VECTOR ( 'NONE', #1973, 1000.000000000000114 ) ;
#12580=VERTEX_POINT ( 'NONE', #3932 ) ;
#12593=FACE_OUTER_BOUND ( 'NONE', #6737, .T. ) ;
#12602=EDGE_CURVE ( 'NONE', #2398, #10844, #4964, .T. ) ;
#12621=LINE ( 'NONE', #2677, #2060 ) ;
#12622=DIRECTION ( 'NONE',  ( 0.000000000000000000, 0.000000000000000000, 1.000000000000000000 ) ) ;
#12643=EDGE_CURVE ( 'NONE', #2484, #7067, #365, .T. ) ;
#12659=DIRECTION ( 'NONE',  ( 0.000000000000000000, 0.000000000000000000, 1.000000000000000000 ) ) ;
#12663=ADVANCED_FACE ( 'NONE', ( #5153 ), #3340, .F. ) ;
#12685=FACE_BOUND ( 'NONE', #423, .T. ) ;
#12691=AXIS2_PLACEMENT_3D ( 'NONE', #10174, #6248, #8350 ) ;
#12753=ORIENTED_EDGE ( 'NONE', *, *, #6043, .T. ) ;
#12794=EDGE_CURVE ( 'NONE', #11762, #5032, #496, .T. ) ;
#12825=( GEOMETRIC_REPRESENTATION_CONTEXT ( 3 ) GLOBAL_UNCERTAINTY_ASSIGNED_CONTEXT ( ( #2121 ) ) GLOBAL_UNIT_ASSIGNED_CONTEXT ( ( #3271, #10449, #12550 ) ) REPRESENTATION_CONTEXT ( 'NONE', 'WORKASPACE' ) );
#12829=ORIENTED_EDGE ( 'NONE', *, *, #12602, .F. ) ;
#12869=EDGE_CURVE ( 'NONE', #12039, #8524, #3594, .T. ) ;
#12884=ORIENTED_EDGE ( 'NONE', *, *, #12794, .T. ) ;
#12911=CARTESIAN_POINT ( 'NONE',  ( 7.369500000000001272, 1.836970198721029934E-16, -1.500000000000000000 ) ) ;
#12919=VECTOR ( 'NONE', #10911, 1000.000000000000114 ) ;
#13003=COLOUR_RGB('Black',0.12,0.14,0.17);
#13004=FILL_AREA_STYLE_COLOUR('',#13003);
#13005=FILL_AREA_STYLE('',(#13004));
#13006=SURFACE_STYLE_FILL_AREA(#13005);
#13007=SURFACE_SIDE_STYLE('',(#13006));
#13008=SURFACE_STYLE_USAGE(.BOTH.,#13007);
#13009=PRESENTATION_STYLE_ASSIGNMENT((#13008));
ENDSEC;
END-ISO-10303-21;
